ISO-10303-21;
HEADER;
FILE_DESCRIPTION (('STEP AP214'),
    '1' );
FILE_NAME ('Thermostate Flange.step',
    '2026-10-23T18:01:19',
    ( '' ),
    ( '' ),
    'SwSTEP 2.0',
    'SolidWorks 2025',
    '' );
FILE_SCHEMA (( 'AUTOMOTIVE_DESIGN' ));
ENDSEC;

DATA;
#27=ORIENTED_EDGE ( 'NONE', *, *, #241, .F. ) ;
#28=EDGE_CURVE ( 'NONE', #11196, #3954, #11572, .T. ) ;
#32=CARTESIAN_POINT ( 'NONE',  ( 3.874999999999999556, 3.567999999999999616, -1.320000000000000062 ) ) ;
#50=DIRECTION ( 'NONE',  ( 0.000000000000000000, 0.000000000000000000, 1.000000000000000000 ) ) ;
#51=AXIS2_PLACEMENT_3D ( 'NONE', #8937, #9020, #9933 ) ;
#84=DIRECTION ( 'NONE',  ( -0.000000000000000000, -1.000000000000000000, -0.000000000000000000 ) ) ;
#121=CIRCLE ( 'NONE', #850, 0.1899999999999996136 ) ;
#165=CARTESIAN_POINT ( 'NONE',  ( 3.874999999999999556, 3.567999999999999616, -1.320000000000000062 ) ) ;
#174=EDGE_CURVE ( 'NONE', #282, #4996, #14362, .T. ) ;
#179=CONICAL_SURFACE ( 'NONE', #7293, 0.5174999999999995159, 0.7853981633974514986 ) ;
#199=FACE_OUTER_BOUND ( 'NONE', #10241, .T. ) ;
#234=CARTESIAN_POINT ( 'NONE',  ( 3.874999999999999556, 3.567999999999999616, -1.130000000000000560 ) ) ;
#241=EDGE_CURVE ( 'NONE', #287, #6694, #6272, .T. ) ;
#267=DIRECTION ( 'NONE',  ( 0.000000000000000000, 0.000000000000000000, -1.000000000000000000 ) ) ;
#281=DIRECTION ( 'NONE',  ( -0.9396926207859105373, 0.000000000000000000, 0.3420201433256627732 ) ) ;
#282=VERTEX_POINT ( 'NONE', #8788 ) ;
#287=VERTEX_POINT ( 'NONE', #11147 ) ;
#292=ORIENTED_EDGE ( 'NONE', *, *, #11564, .F. ) ;
#318=DIRECTION ( 'NONE',  ( -0.000000000000000000, -1.000000000000000000, -0.000000000000000000 ) ) ;
#324=ADVANCED_FACE ( 'NONE', ( #14504 ), #6670, .F. ) ;
#350=DIRECTION ( 'NONE',  ( 0.000000000000000000, 1.000000000000000000, 0.000000000000000000 ) ) ;
#356=EDGE_CURVE ( 'NONE', #5312, #13169, #5450, .T. ) ;
#376=CARTESIAN_POINT ( 'NONE',  ( 4.769268701363833074, 3.137999999999999901, -0.3249191361593797289 ) ) ;
#388=DIMENSIONAL_EXPONENTS ( 1.000000000000000000, 0.000000000000000000, 0.000000000000000000, 0.000000000000000000, 0.000000000000000000, 0.000000000000000000, 0.000000000000000000 ) ;
#415=AXIS2_PLACEMENT_3D ( 'NONE', #5979, #1448, #8366 ) ;
#422=EDGE_CURVE ( 'NONE', #10962, #11613, #2463, .T. ) ;
#446=LINE ( 'NONE', #2921, #8765 ) ;
#467=AXIS2_PLACEMENT_3D ( 'NONE', #10705, #1433, #10781 ) ;
#491=MANIFOLD_SOLID_BREP ( 'Chamfer5', #14246 ) ;
#493=PLANE ( 'NONE',  #11640 ) ;
#500=ORIENTED_EDGE ( 'NONE', *, *, #14271, .T. ) ;
#512=DIRECTION ( 'NONE',  ( 0.000000000000000000, 0.000000000000000000, 1.000000000000000000 ) ) ;
#523=DIRECTION ( 'NONE',  ( 0.000000000000000000, 0.000000000000000000, -1.000000000000000000 ) ) ;
#526=ORIENTED_EDGE ( 'NONE', *, *, #5349, .F. ) ;
#559=CARTESIAN_POINT ( 'NONE',  ( 3.875000000000000000, 3.137999999999999901, -0.5174999999999995159 ) ) ;
#570=ORIENTED_EDGE ( 'NONE', *, *, #28, .T. ) ;
#588=CARTESIAN_POINT ( 'NONE',  ( 2.980731298636167370, 3.137999999999999901, 0.3249191361593796734 ) ) ;
#594=DIRECTION ( 'NONE',  ( -0.000000000000000000, -1.000000000000000000, -0.000000000000000000 ) ) ;
#606=ADVANCED_FACE ( 'NONE', ( #1000 ), #6674, .F. ) ;
#620=ORIENTED_EDGE ( 'NONE', *, *, #7740, .F. ) ;
#643=PRODUCT_DEFINITION_SHAPE ( 'NONE', 'NONE',  #869 ) ;
#653=EDGE_LOOP ( 'NONE', ( #4006, #1589, #12203, #1711 ) ) ;
#659=CARTESIAN_POINT ( 'NONE',  ( 4.769268701363833074, 3.137999999999999901, -0.3249191361593797289 ) ) ;
#675=CYLINDRICAL_SURFACE ( 'NONE', #1096, 0.5000000000000001110 ) ;
#678=DIRECTION ( 'NONE',  ( -0.000000000000000000, -1.000000000000000000, -0.000000000000000000 ) ) ;
#683=DIRECTION ( 'NONE',  ( 0.000000000000000000, -0.7071067811865500152, -0.7071067811865449082 ) ) ;
#696=EDGE_CURVE ( 'NONE', #13169, #12132, #10427, .T. ) ;
#723=FACE_OUTER_BOUND ( 'NONE', #3702, .T. ) ;
#739=CARTESIAN_POINT ( 'NONE',  ( 3.874999999999999556, 3.170500000000000096, 1.320000000000000062 ) ) ;
#754=VERTEX_POINT ( 'NONE', #12861 ) ;
#776=AXIS2_PLACEMENT_3D ( 'NONE', #12632, #5620, #13700 ) ;
#794=AXIS2_PLACEMENT_3D ( 'NONE', #10044, #678, #9045 ) ;
#799=VERTEX_POINT ( 'NONE', #14529 ) ;
#801=VERTEX_POINT ( 'NONE', #11094 ) ;
#818=EDGE_LOOP ( 'NONE', ( #5751, #3194 ) ) ;
#819=DIRECTION ( 'NONE',  ( 0.3420201433256620516, 0.000000000000000000, 0.9396926207859108704 ) ) ;
#821=CARTESIAN_POINT ( 'NONE',  ( 3.874999999999999556, 3.567999999999999616, -1.820000000000000284 ) ) ;
#825=ORIENTED_EDGE ( 'NONE', *, *, #7407, .T. ) ;
#849=EDGE_CURVE ( 'NONE', #7678, #799, #9607, .T. ) ;
#850=AXIS2_PLACEMENT_3D ( 'NONE', #3235, #7900, #12551 ) ;
#860=ORIENTED_EDGE ( 'NONE', *, *, #4113, .T. ) ;
#869=PRODUCT_DEFINITION ( 'UNKNOWN', '', #12798, #3254 ) ;
#921=CIRCLE ( 'NONE', #11927, 0.5000000000000000000 ) ;
#923=FACE_OUTER_BOUND ( 'NONE', #1949, .T. ) ;
#926=DIRECTION ( 'NONE',  ( 0.000000000000000000, -0.7071067811865501263, -0.7071067811865449082 ) ) ;
#952=EDGE_LOOP ( 'NONE', ( #12292, #10995, #9837, #7098 ) ) ;
#956=CIRCLE ( 'NONE', #10758, 0.5000000000000000000 ) ;
#975=EDGE_CURVE ( 'NONE', #9328, #8969, #4295, .T. ) ;
#989=LINE ( 'NONE', #9433, #5615 ) ;
#995=EDGE_CURVE ( 'NONE', #11613, #10962, #8387, .T. ) ;
#1000=FACE_OUTER_BOUND ( 'NONE', #10425, .T. ) ;
#1034=ORIENTED_EDGE ( 'NONE', *, *, #7995, .F. ) ;
#1038=CARTESIAN_POINT ( 'NONE',  ( 3.874999999999999556, 3.170500000000001428, -1.130000000000000560 ) ) ;
#1041=CARTESIAN_POINT ( 'NONE',  ( 4.344846310392954436, 3.567999999999999616, 1.491010071662831393 ) ) ;
#1049=DIRECTION ( 'NONE',  ( 0.000000000000000000, 0.000000000000000000, 1.000000000000000000 ) ) ;
#1072=EDGE_LOOP ( 'NONE', ( #4283, #12804 ) ) ;
#1078=ORIENTED_EDGE ( 'NONE', *, *, #4120, .F. ) ;
#1096=AXIS2_PLACEMENT_3D ( 'NONE', #2994, #3927, #523 ) ;
#1172=ORIENTED_EDGE ( 'NONE', *, *, #1481, .F. ) ;
#1212=DIRECTION ( 'NONE',  ( 0.000000000000000000, 0.000000000000000000, 1.000000000000000000 ) ) ;
#1221=LINE ( 'NONE', #1292, #1649 ) ;
#1225=ADVANCED_FACE ( 'NONE', ( #2621 ), #8300, .F. ) ;
#1226=EDGE_CURVE ( 'NONE', #4411, #3185, #446, .T. ) ;
#1259=CARTESIAN_POINT ( 'NONE',  ( 3.874999999999999556, 3.535499999999999421, -1.320000000000000062 ) ) ;
#1287=ORIENTED_EDGE ( 'NONE', *, *, #12402, .F. ) ;
#1292=CARTESIAN_POINT ( 'NONE',  ( 2.980731298636167370, 3.567999999999999616, 0.3249191361593796179 ) ) ;
#1323=ORIENTED_EDGE ( 'NONE', *, *, #5681, .T. ) ;
#1332=AXIS2_PLACEMENT_3D ( 'NONE', #13543, #4164, #13625 ) ;
#1345=FACE_OUTER_BOUND ( 'NONE', #3353, .T. ) ;
#1363=EDGE_CURVE ( 'NONE', #799, #11919, #10951, .T. ) ;
#1364=DIRECTION ( 'NONE',  ( -0.000000000000000000, -1.000000000000000000, -0.000000000000000000 ) ) ;
#1365=DIRECTION ( 'NONE',  ( 0.000000000000000000, 1.000000000000000000, 0.000000000000000000 ) ) ;
#1392=VECTOR ( 'NONE', #8781, 39.37007874015748143 ) ;
#1433=DIRECTION ( 'NONE',  ( 0.000000000000000000, 1.000000000000000000, 0.000000000000000000 ) ) ;
#1448=DIRECTION ( 'NONE',  ( -0.000000000000000000, -1.000000000000000000, -0.000000000000000000 ) ) ;
#1465=AXIS2_PLACEMENT_3D ( 'NONE', #14897, #11605, #4725 ) ;
#1466=CARTESIAN_POINT ( 'NONE',  ( 3.874999999999999556, 3.535499999999999421, 1.509999999999999787 ) ) ;
#1480=EDGE_LOOP ( 'NONE', ( #14975, #7023, #500, #8833 ) ) ;
#1481=EDGE_CURVE ( 'NONE', #12926, #7285, #11319, .T. ) ;
#1521=DIRECTION ( 'NONE',  ( 1.000000000000000000, 0.000000000000000000, 0.000000000000000000 ) ) ;
#1543=CARTESIAN_POINT ( 'NONE',  ( 3.875000000000000000, 3.137999999999999901, 0.000000000000000000 ) ) ;
#1549=ORIENTED_EDGE ( 'NONE', *, *, #6080, .T. ) ;
#1586=ORIENTED_EDGE ( 'NONE', *, *, #6661, .F. ) ;
#1589=ORIENTED_EDGE ( 'NONE', *, *, #10671, .T. ) ;
#1614=AXIS2_PLACEMENT_3D ( 'NONE', #12574, #13489, #6634 ) ;
#1626=CARTESIAN_POINT ( 'NONE',  ( 4.344846310392954436, 3.567999999999999616, -1.491010071662831171 ) ) ;
#1642=LINE ( 'NONE', #13339, #6042 ) ;
#1645=CARTESIAN_POINT ( 'NONE',  ( 3.874999999999999556, 3.567999999999999616, -1.320000000000000062 ) ) ;
#1649=VECTOR ( 'NONE', #7357, 39.37007874015748143 ) ;
#1711=ORIENTED_EDGE ( 'NONE', *, *, #12290, .T. ) ;
#1727=DIRECTION ( 'NONE',  ( 0.000000000000000000, 0.000000000000000000, 1.000000000000000000 ) ) ;
#1748=DIRECTION ( 'NONE',  ( -0.000000000000000000, -1.000000000000000000, -0.000000000000000000 ) ) ;
#1788=ORIENTED_EDGE ( 'NONE', *, *, #12454, .T. ) ;
#1789=LINE ( 'NONE', #4414, #6289 ) ;
#1803=DIRECTION ( 'NONE',  ( 0.000000000000000000, 1.000000000000000000, 0.000000000000000000 ) ) ;
#1831=DIRECTION ( 'NONE',  ( 0.000000000000000000, 1.000000000000000000, 0.000000000000000000 ) ) ;
#1840=AXIS2_PLACEMENT_3D ( 'NONE', #1985, #1365, #12767 ) ;
#1844=VECTOR ( 'NONE', #14742, 39.37007874015748143 ) ;
#1851=ORIENTED_EDGE ( 'NONE', *, *, #10999, .F. ) ;
#1858=CARTESIAN_POINT ( 'NONE',  ( 3.875000000000000000, 3.535499999999999865, 0.000000000000000000 ) ) ;
#1879=DIRECTION ( 'NONE',  ( -0.000000000000000000, -1.000000000000000000, -0.000000000000000000 ) ) ;
#1942=CARTESIAN_POINT ( 'NONE',  ( 3.875000000000000000, 3.170499999999999208, 0.4849999999999995981 ) ) ;
#1944=ORIENTED_EDGE ( 'NONE', *, *, #7030, .T. ) ;
#1949=EDGE_LOOP ( 'NONE', ( #8429, #14296, #3758, #2440 ) ) ;
#1985=CARTESIAN_POINT ( 'NONE',  ( 3.874999999999999556, 3.535499999999999421, 1.320000000000000062 ) ) ;
#1990=CARTESIAN_POINT ( 'NONE',  ( 3.874999999999999556, 3.535499999999999421, 1.320000000000000062 ) ) ;
#2002=DIRECTION ( 'NONE',  ( 0.9396926207859108704, -0.000000000000000000, 0.3420201433256621626 ) ) ;
#2017=ORIENTED_EDGE ( 'NONE', *, *, #12262, .F. ) ;
#2019=CYLINDRICAL_SURFACE ( 'NONE', #1614, 0.9499999999999988454 ) ;
#2026=CIRCLE ( 'NONE', #3767, 0.5175000000000000711 ) ;
#2068=DIRECTION ( 'NONE',  ( 0.000000000000000000, 0.000000000000000000, 1.000000000000000000 ) ) ;
#2078=CARTESIAN_POINT ( 'NONE',  ( 3.874999999999999556, 3.137999999999999901, -1.542500000000001315 ) ) ;
#2081=CARTESIAN_POINT ( 'NONE',  ( 2.980731298636167370, 3.137999999999999901, -0.3249191361593797844 ) ) ;
#2094=CIRCLE ( 'NONE', #4312, 0.1899999999999996136 ) ;
#2105=VECTOR ( 'NONE', #3669, 39.37007874015748143 ) ;
#2108=CARTESIAN_POINT ( 'NONE',  ( 3.874999999999999556, 3.567999999999999616, -1.820000000000000284 ) ) ;
#2109=DIRECTION ( 'NONE',  ( 0.000000000000000000, 0.000000000000000000, 1.000000000000000000 ) ) ;
#2198=EDGE_LOOP ( 'NONE', ( #1788, #15041, #6470, #8160 ) ) ;
#2228=DIRECTION ( 'NONE',  ( 8.659560562354900811E-17, -0.7071067811865500152, 0.7071067811865449082 ) ) ;
#2243=EDGE_LOOP ( 'NONE', ( #12112, #620, #6494, #2715 ) ) ;
#2275=PLANE ( 'NONE',  #3343 ) ;
#2279=CIRCLE ( 'NONE', #13019, 0.2225000000000001421 ) ;
#2302=CIRCLE ( 'NONE', #6223, 0.5000000000000001110 ) ;
#2361=EDGE_CURVE ( 'NONE', #13169, #10530, #11713, .T. ) ;
#2395=DIRECTION ( 'NONE',  ( 8.659560562354959975E-17, -0.7071067811865452413, 0.7071067811865496822 ) ) ;
#2402=CYLINDRICAL_SURFACE ( 'NONE', #6006, 0.1899999999999996136 ) ;
#2434=AXIS2_PLACEMENT_3D ( 'NONE', #3654, #14033, #7175 ) ;
#2440=ORIENTED_EDGE ( 'NONE', *, *, #11014, .F. ) ;
#2444=DIRECTION ( 'NONE',  ( -0.000000000000000000, -1.000000000000000000, -0.000000000000000000 ) ) ;
#2451=CARTESIAN_POINT ( 'NONE',  ( 3.875000000000000000, 3.137999999999999901, 0.000000000000000000 ) ) ;
#2463=CIRCLE ( 'NONE', #1465, 0.2224999999999996148 ) ;
#2488=EDGE_LOOP ( 'NONE', ( #4732, #7802 ) ) ;
#2530=CARTESIAN_POINT ( 'NONE',  ( 4.769268701363833074, 3.567999999999999616, -0.3249191361593797289 ) ) ;
#2543=EDGE_LOOP ( 'NONE', ( #11950, #526, #292, #6137 ) ) ;
#2621=FACE_OUTER_BOUND ( 'NONE', #3128, .T. ) ;
#2647=VECTOR ( 'NONE', #9467, 39.37007874015748143 ) ;
#2650=APPLICATION_CONTEXT ( 'automotive_design' ) ;
#2656=EDGE_CURVE ( 'NONE', #3185, #11461, #4197, .T. ) ;
#2662=ORIENTED_EDGE ( 'NONE', *, *, #11568, .T. ) ;
#2665=DIRECTION ( 'NONE',  ( 0.000000000000000000, -0.7071067811865452413, -0.7071067811865496822 ) ) ;
#2666=PRODUCT_CONTEXT ( 'NONE', #2650, 'mechanical' ) ;
#2693=ADVANCED_FACE ( 'NONE', ( #723 ), #9443, .F. ) ;
#2713=FACE_OUTER_BOUND ( 'NONE', #3435, .T. ) ;
#2714=VECTOR ( 'NONE', #1879, 39.37007874015748143 ) ;
#2715=ORIENTED_EDGE ( 'NONE', *, *, #7536, .F. ) ;
#2718=ADVANCED_FACE ( 'NONE', ( #6347 ), #493, .F. ) ;
#2754=CARTESIAN_POINT ( 'NONE',  ( 2.980731298636167370, 3.567999999999999616, 0.3249191361593796179 ) ) ;
#2769=FACE_OUTER_BOUND ( 'NONE', #4960, .T. ) ;
#2770=ORIENTED_EDGE ( 'NONE', *, *, #12262, .T. ) ;
#2824=ORIENTED_EDGE ( 'NONE', *, *, #7030, .F. ) ;
#2856=EDGE_CURVE ( 'NONE', #6694, #5312, #10178, .T. ) ;
#2863=AXIS2_PLACEMENT_3D ( 'NONE', #14207, #5963, #267 ) ;
#2883=LINE ( 'NONE', #13202, #1392 ) ;
#2892=CIRCLE ( 'NONE', #7534, 0.1899999999999996136 ) ;
#2921=CARTESIAN_POINT ( 'NONE',  ( 4.344846310392954436, 3.567999999999999616, 1.491010071662831393 ) ) ;
#2932=FACE_OUTER_BOUND ( 'NONE', #10822, .T. ) ;
#2934=FACE_OUTER_BOUND ( 'NONE', #5759, .T. ) ;
#2937=CARTESIAN_POINT ( 'NONE',  ( 3.874999999999999556, 3.137999999999999901, -1.820000000000000284 ) ) ;
#2939=ORIENTED_EDGE ( 'NONE', *, *, #5112, .F. ) ;
#2962=ADVANCED_FACE ( 'NONE', ( #10816 ), #3302, .F. ) ;
#2968=ADVANCED_FACE ( 'NONE', ( #2934 ), #10972, .F. ) ;
#2970=DIRECTION ( 'NONE',  ( 0.000000000000000000, 1.000000000000000000, 0.000000000000000000 ) ) ;
#2994=CARTESIAN_POINT ( 'NONE',  ( 3.874999999999999556, 3.567999999999999616, -1.320000000000000062 ) ) ;
#3016=CARTESIAN_POINT ( 'NONE',  ( 3.874999999999999556, 3.567999999999999616, 1.130000000000000560 ) ) ;
#3027=DIRECTION ( 'NONE',  ( -0.000000000000000000, -1.000000000000000000, -0.000000000000000000 ) ) ;
#3032=ORIENTED_EDGE ( 'NONE', *, *, #174, .T. ) ;
#3037=CARTESIAN_POINT ( 'NONE',  ( 3.874999999999999556, 3.535499999999999421, -1.509999999999999787 ) ) ;
#3042=ADVANCED_FACE ( 'NONE', ( #2713 ), #5688, .F. ) ;
#3049=EDGE_LOOP ( 'NONE', ( #10057, #8350, #12397, #9722 ) ) ;
#3053=DIRECTION ( 'NONE',  ( 0.000000000000000000, 0.000000000000000000, -1.000000000000000000 ) ) ;
#3089=ORIENTED_EDGE ( 'NONE', *, *, #9889, .F. ) ;
#3128=EDGE_LOOP ( 'NONE', ( #6619, #14044, #9370, #13549 ) ) ;
#3165=FACE_OUTER_BOUND ( 'NONE', #5079, .T. ) ;
#3175=VERTEX_POINT ( 'NONE', #12409 ) ;
#3185=VERTEX_POINT ( 'NONE', #7749 ) ;
#3194=ORIENTED_EDGE ( 'NONE', *, *, #7003, .T. ) ;
#3205=VERTEX_POINT ( 'NONE', #5699 ) ;
#3219=LINE ( 'NONE', #821, #5009 ) ;
#3235=CARTESIAN_POINT ( 'NONE',  ( 3.874999999999999556, 3.170500000000000096, 1.320000000000000062 ) ) ;
#3254=PRODUCT_DEFINITION_CONTEXT ( 'detailed design', #8901, 'design' ) ;
#3262=DIRECTION ( 'NONE',  ( 0.000000000000000000, 0.000000000000000000, 1.000000000000000000 ) ) ;
#3268=DIRECTION ( 'NONE',  ( 0.000000000000000000, 1.000000000000000000, 0.000000000000000000 ) ) ;
#3302=CONICAL_SURFACE ( 'NONE', #4026, 0.2225000000000012523, 0.7853981633974446153 ) ;
#3328=ORIENTED_EDGE ( 'NONE', *, *, #9735, .F. ) ;
#3341=ADVANCED_FACE ( 'NONE', ( #12870 ), #2402, .F. ) ;
#3343=AXIS2_PLACEMENT_3D ( 'NONE', #9483, #6959, #3740 ) ;
#3353=EDGE_LOOP ( 'NONE', ( #9115, #10416, #2824, #10004, #9741, #1172, #13864, #8449, #2017 ) ) ;
#3362=CARTESIAN_POINT ( 'NONE',  ( 3.874999999999999556, 3.137999999999999901, -1.320000000000000062 ) ) ;
#3363=DIRECTION ( 'NONE',  ( -0.000000000000000000, -1.000000000000000000, -0.000000000000000000 ) ) ;
#3378=ORIENTED_EDGE ( 'NONE', *, *, #1363, .T. ) ;
#3381=EDGE_CURVE ( 'NONE', #12094, #8206, #6586, .T. ) ;
#3384=DIRECTION ( 'NONE',  ( 0.000000000000000000, 1.000000000000000000, 0.000000000000000000 ) ) ;
#3422=DIRECTION ( 'NONE',  ( 0.000000000000000000, 0.000000000000000000, 1.000000000000000000 ) ) ;
#3435=EDGE_LOOP ( 'NONE', ( #8390, #3378, #8525, #3718 ) ) ;
#3443=CIRCLE ( 'NONE', #8819, 0.1899999999999996136 ) ;
#3451=CARTESIAN_POINT ( 'NONE',  ( 3.875000000000000000, 3.567999999999999616, 0.000000000000000000 ) ) ;
#3469=DIRECTION ( 'NONE',  ( 0.000000000000000000, 1.000000000000000000, 0.000000000000000000 ) ) ;
#3473=ORIENTED_EDGE ( 'NONE', *, *, #6420, .F. ) ;
#3513=AXIS2_PLACEMENT_3D ( 'NONE', #2451, #13828, #1212 ) ;
#3541=ORIENTED_EDGE ( 'NONE', *, *, #2361, .F. ) ;
#3588=FACE_BOUND ( 'NONE', #2488, .T. ) ;
#3590=DIRECTION ( 'NONE',  ( 0.000000000000000000, 0.000000000000000000, -1.000000000000000000 ) ) ;
#3654=CARTESIAN_POINT ( 'NONE',  ( 3.874999999999999556, 3.535499999999999421, 1.320000000000000062 ) ) ;
#3669=DIRECTION ( 'NONE',  ( -0.000000000000000000, -1.000000000000000000, -0.000000000000000000 ) ) ;
#3685=SHAPE_REPRESENTATION ( 'Thermostate Flange', ( #8424 ), #12311 ) ;
#3687=CYLINDRICAL_SURFACE ( 'NONE', #14315, 0.5000000000000000000 ) ;
#3702=EDGE_LOOP ( 'NONE', ( #1287, #860, #3328, #6038 ) ) ;
#3713=ADVANCED_FACE ( 'NONE', ( #12831 ), #6542, .F. ) ;
#3718=ORIENTED_EDGE ( 'NONE', *, *, #8218, .F. ) ;
#3719=CARTESIAN_POINT ( 'NONE',  ( 3.874999999999999556, 3.567999999999999616, -1.509999999999999787 ) ) ;
#3740=DIRECTION ( 'NONE',  ( 0.000000000000000000, -0.000000000000000000, 1.000000000000000000 ) ) ;
#3758=ORIENTED_EDGE ( 'NONE', *, *, #7836, .F. ) ;
#3760=DIRECTION ( 'NONE',  ( 0.000000000000000000, 1.000000000000000000, 0.000000000000000000 ) ) ;
#3767=AXIS2_PLACEMENT_3D ( 'NONE', #12690, #3363, #50 ) ;
#3803=ORIENTED_EDGE ( 'NONE', *, *, #6420, .T. ) ;
#3805=DIRECTION ( 'NONE',  ( 0.000000000000000000, 1.000000000000000000, 0.000000000000000000 ) ) ;
#3853=DIRECTION ( 'NONE',  ( 0.000000000000000000, 0.000000000000000000, 1.000000000000000000 ) ) ;
#3869=EDGE_CURVE ( 'NONE', #12094, #8646, #2883, .T. ) ;
#3896=DIRECTION ( 'NONE',  ( 0.000000000000000000, 0.000000000000000000, 1.000000000000000000 ) ) ;
#3897=CIRCLE ( 'NONE', #10249, 0.4849999999999995981 ) ;
#3927=DIRECTION ( 'NONE',  ( -0.000000000000000000, -1.000000000000000000, -0.000000000000000000 ) ) ;
#3944=CARTESIAN_POINT ( 'NONE',  ( 3.875000000000000000, 3.170499999999999208, -0.4849999999999995981 ) ) ;
#3954=VERTEX_POINT ( 'NONE', #559 ) ;
#3976=ORIENTED_EDGE ( 'NONE', *, *, #5112, .T. ) ;
#3978=DIRECTION ( 'NONE',  ( 0.000000000000000000, 0.7071067811865392461, 0.7071067811865555663 ) ) ;
#3979=AXIS2_PLACEMENT_3D ( 'NONE', #32, #3268, #2109 ) ;
#3984=DIRECTION ( 'NONE',  ( -0.000000000000000000, -1.000000000000000000, -0.000000000000000000 ) ) ;
#4006=ORIENTED_EDGE ( 'NONE', *, *, #1363, .F. ) ;
#4026=AXIS2_PLACEMENT_3D ( 'NONE', #5014, #8745, #7520 ) ;
#4051=( NAMED_UNIT ( * ) PLANE_ANGLE_UNIT ( ) SI_UNIT ( $, .RADIAN. ) );
#4062=DIRECTION ( 'NONE',  ( 0.000000000000000000, 0.000000000000000000, -1.000000000000000000 ) ) ;
#4067=FACE_OUTER_BOUND ( 'NONE', #952, .T. ) ;
#4086=EDGE_CURVE ( 'NONE', #12132, #9328, #4598, .T. ) ;
#4102=ORIENTED_EDGE ( 'NONE', *, *, #10637, .T. ) ;
#4113=EDGE_CURVE ( 'NONE', #5284, #6726, #9159, .T. ) ;
#4120=EDGE_CURVE ( 'NONE', #8206, #5828, #8282, .T. ) ;
#4154=DIRECTION ( 'NONE',  ( 0.000000000000000000, 0.000000000000000000, 1.000000000000000000 ) ) ;
#4164=DIRECTION ( 'NONE',  ( -0.000000000000000000, -1.000000000000000000, -0.000000000000000000 ) ) ;
#4178=EDGE_CURVE ( 'NONE', #9328, #12926, #1221, .T. ) ;
#4193=LINE ( 'NONE', #12364, #2714 ) ;
#4197=LINE ( 'NONE', #8860, #1844 ) ;
#4208=SHAPE_REPRESENTATION_RELATIONSHIP ( 'NONE' , 'NONE' ,  #3685, #12215 ) ;
#4273=DIRECTION ( 'NONE',  ( 0.000000000000000000, -0.000000000000000000, 1.000000000000000000 ) ) ;
#4275=AXIS2_PLACEMENT_3D ( 'NONE', #1990, #3384, #2068 ) ;
#4279=ORIENTED_EDGE ( 'NONE', *, *, #696, .T. ) ;
#4283=ORIENTED_EDGE ( 'NONE', *, *, #11591, .T. ) ;
#4293=ORIENTED_EDGE ( 'NONE', *, *, #14542, .F. ) ;
#4295=LINE ( 'NONE', #6514, #11048 ) ;
#4297=ORIENTED_EDGE ( 'NONE', *, *, #6342, .F. ) ;
#4301=AXIS2_PLACEMENT_3D ( 'NONE', #13499, #8934, #9932 ) ;
#4312=AXIS2_PLACEMENT_3D ( 'NONE', #10208, #4321, #4398 ) ;
#4321=DIRECTION ( 'NONE',  ( -0.000000000000000000, -1.000000000000000000, -0.000000000000000000 ) ) ;
#4385=DIRECTION ( 'NONE',  ( 0.000000000000000000, 1.000000000000000000, 0.000000000000000000 ) ) ;
#4388=VECTOR ( 'NONE', #11030, 39.37007874015748143 ) ;
#4398=DIRECTION ( 'NONE',  ( 0.000000000000000000, 0.000000000000000000, 1.000000000000000000 ) ) ;
#4411=VERTEX_POINT ( 'NONE', #1041 ) ;
#4414=CARTESIAN_POINT ( 'NONE',  ( 3.874999999999999556, 3.567999999999999616, 1.509999999999999787 ) ) ;
#4453=ADVANCED_FACE ( 'NONE', ( #6034, #3588, #5957, #1345 ), #2275, .F. ) ;
#4497=FACE_BOUND ( 'NONE', #6368, .T. ) ;
#4528=AXIS2_PLACEMENT_3D ( 'NONE', #165, #4867, #9605 ) ;
#4560=ORIENTED_EDGE ( 'NONE', *, *, #6861, .T. ) ;
#4576=DIRECTION ( 'NONE',  ( -0.000000000000000000, -1.000000000000000000, -0.000000000000000000 ) ) ;
#4592=EDGE_CURVE ( 'NONE', #5059, #3954, #1642, .T. ) ;
#4598=CIRCLE ( 'NONE', #12640, 0.9499999999999988454 ) ;
#4668=CARTESIAN_POINT ( 'NONE',  ( 3.874999999999999556, 3.137999999999999901, 1.097500000000000586 ) ) ;
#4712=LINE ( 'NONE', #3719, #14796 ) ;
#4716=VECTOR ( 'NONE', #10931, 39.37007874015748143 ) ;
#4725=DIRECTION ( 'NONE',  ( 0.000000000000000000, 0.000000000000000000, 1.000000000000000000 ) ) ;
#4730=EDGE_LOOP ( 'NONE', ( #14344, #2939, #27, #4102 ) ) ;
#4732=ORIENTED_EDGE ( 'NONE', *, *, #422, .T. ) ;
#4741=DIRECTION ( 'NONE',  ( 0.000000000000000000, 1.000000000000000000, 0.000000000000000000 ) ) ;
#4743=CARTESIAN_POINT ( 'NONE',  ( 3.405153689607044232, 3.567999999999999616, -1.491010071662831171 ) ) ;
#4761=ADVANCED_FACE ( 'NONE', ( #12657 ), #2019, .T. ) ;
#4778=DIRECTION ( 'NONE',  ( 0.000000000000000000, 0.000000000000000000, -1.000000000000000000 ) ) ;
#4804=AXIS2_PLACEMENT_3D ( 'NONE', #3451, #11788, #4911 ) ;
#4816=SHAPE_DEFINITION_REPRESENTATION ( #643, #3685 ) ;
#4852=DIRECTION ( 'NONE',  ( -0.3420201433256621071, 0.000000000000000000, 0.9396926207859108704 ) ) ;
#4867=DIRECTION ( 'NONE',  ( 0.000000000000000000, 1.000000000000000000, 0.000000000000000000 ) ) ;
#4872=ORIENTED_EDGE ( 'NONE', *, *, #10706, .T. ) ;
#4911=DIRECTION ( 'NONE',  ( 0.000000000000000000, 0.000000000000000000, 1.000000000000000000 ) ) ;
#4960=EDGE_LOOP ( 'NONE', ( #10575, #13359, #2770, #3541 ) ) ;
#4973=CARTESIAN_POINT ( 'NONE',  ( 2.980731298636167370, 3.567999999999999616, 0.3249191361593796734 ) ) ;
#4996=VERTEX_POINT ( 'NONE', #10904 ) ;
#5003=LINE ( 'NONE', #5995, #14435 ) ;
#5009=VECTOR ( 'NONE', #11481, 39.37007874015748143 ) ;
#5014=CARTESIAN_POINT ( 'NONE',  ( 3.874999999999999556, 3.137999999999999901, -1.320000000000000062 ) ) ;
#5059=VERTEX_POINT ( 'NONE', #3944 ) ;
#5062=CARTESIAN_POINT ( 'NONE',  ( 0.000000000000000000, 0.000000000000000000, 0.000000000000000000 ) ) ;
#5063=CARTESIAN_POINT ( 'NONE',  ( 3.875000000000000000, 3.567999999999999616, 0.000000000000000000 ) ) ;
#5079=EDGE_LOOP ( 'NONE', ( #14353, #3032, #10143, #3089 ) ) ;
#5082=CARTESIAN_POINT ( 'NONE',  ( 2.980731298636167370, 3.567999999999999616, -0.3249191361593797844 ) ) ;
#5099=VECTOR ( 'NONE', #3978, 39.37007874015748854 ) ;
#5104=VECTOR ( 'NONE', #3984, 39.37007874015748143 ) ;
#5112=EDGE_CURVE ( 'NONE', #6694, #754, #12046, .T. ) ;
#5147=CARTESIAN_POINT ( 'NONE',  ( 3.875000000000000000, 3.567999999999999616, 0.4849999999999995981 ) ) ;
#5172=ADVANCED_FACE ( 'NONE', ( #7761 ), #6690, .F. ) ;
#5203=CARTESIAN_POINT ( 'NONE',  ( 3.874999999999999556, 3.137999999999999901, -1.320000000000000062 ) ) ;
#5215=CARTESIAN_POINT ( 'NONE',  ( 3.874999999999999556, 3.567999999999999616, 1.320000000000000062 ) ) ;
#5230=EDGE_LOOP ( 'NONE', ( #825, #570 ) ) ;
#5241=CARTESIAN_POINT ( 'NONE',  ( 2.980731298636167370, 3.137999999999999901, 0.3249191361593796179 ) ) ;
#5259=DIRECTION ( 'NONE',  ( -0.3420201433256627732, 0.000000000000000000, 0.9396926207859105373 ) ) ;
#5270=EDGE_LOOP ( 'NONE', ( #1851, #4872, #6915, #14680 ) ) ;
#5284=VERTEX_POINT ( 'NONE', #3037 ) ;
#5290=EDGE_LOOP ( 'NONE', ( #1323, #4297, #7160, #8951 ) ) ;
#5308=EDGE_LOOP ( 'NONE', ( #15056, #14065, #4279, #12056, #8441, #8262, #10185, #14923, #6028 ) ) ;
#5312=VERTEX_POINT ( 'NONE', #2108 ) ;
#5316=DIRECTION ( 'NONE',  ( 0.3420201433256621626, 0.000000000000000000, -0.9396926207859108704 ) ) ;
#5323=EDGE_CURVE ( 'NONE', #7678, #801, #13497, .T. ) ;
#5349=EDGE_CURVE ( 'NONE', #3205, #11461, #4193, .T. ) ;
#5358=FACE_OUTER_BOUND ( 'NONE', #653, .T. ) ;
#5379=CYLINDRICAL_SURFACE ( 'NONE', #794, 0.1899999999999996136 ) ;
#5380=LINE ( 'NONE', #6603, #4388 ) ;
#5424=CARTESIAN_POINT ( 'NONE',  ( 3.874999999999999556, 3.535499999999999421, 1.320000000000000062 ) ) ;
#5430=EDGE_CURVE ( 'NONE', #12094, #5284, #3443, .T. ) ;
#5450=CIRCLE ( 'NONE', #3979, 0.5000000000000000000 ) ;
#5497=FACE_BOUND ( 'NONE', #818, .T. ) ;
#5591=DIRECTION ( 'NONE',  ( 0.000000000000000000, 0.000000000000000000, 1.000000000000000000 ) ) ;
#5615=VECTOR ( 'NONE', #2228, 39.37007874015748143 ) ;
#5620=DIRECTION ( 'NONE',  ( -0.000000000000000000, -1.000000000000000000, -0.000000000000000000 ) ) ;
#5637=VERTEX_POINT ( 'NONE', #7079 ) ;
#5645=CARTESIAN_POINT ( 'NONE',  ( 3.874999999999999556, 3.137999999999999901, -1.320000000000000062 ) ) ;
#5681=EDGE_CURVE ( 'NONE', #10530, #9031, #5003, .T. ) ;
#5688=CYLINDRICAL_SURFACE ( 'NONE', #1332, 0.4849999999999995981 ) ;
#5699=CARTESIAN_POINT ( 'NONE',  ( 4.769268701363833074, 3.567999999999999616, 0.3249191361593796734 ) ) ;
#5704=AXIS2_PLACEMENT_3D ( 'NONE', #13666, #2970, #4273 ) ;
#5751=ORIENTED_EDGE ( 'NONE', *, *, #9735, .T. ) ;
#5759=EDGE_LOOP ( 'NONE', ( #10745, #11076, #14309, #13705 ) ) ;
#5769=ORIENTED_EDGE ( 'NONE', *, *, #8994, .F. ) ;
#5828=VERTEX_POINT ( 'NONE', #7180 ) ;
#5833=DIRECTION ( 'NONE',  ( 8.659560562354973534E-17, 0.7071067811865441310, -0.7071067811865509034 ) ) ;
#5867=CIRCLE ( 'NONE', #6123, 0.4849999999999995981 ) ;
#5874=ORIENTED_EDGE ( 'NONE', *, *, #11032, .T. ) ;
#5890=LINE ( 'NONE', #12745, #2105 ) ;
#5909=ORIENTED_EDGE ( 'NONE', *, *, #7003, .F. ) ;
#5946=DIRECTION ( 'NONE',  ( 0.000000000000000000, 1.000000000000000000, 0.000000000000000000 ) ) ;
#5957=FACE_BOUND ( 'NONE', #5230, .T. ) ;
#5963=DIRECTION ( 'NONE',  ( -0.000000000000000000, -1.000000000000000000, -0.000000000000000000 ) ) ;
#5979=CARTESIAN_POINT ( 'NONE',  ( 3.874999999999999556, 3.170500000000001428, -1.320000000000000062 ) ) ;
#5995=CARTESIAN_POINT ( 'NONE',  ( 3.405153689607044232, 3.137999999999999901, -1.491010071662831171 ) ) ;
#6006=AXIS2_PLACEMENT_3D ( 'NONE', #7087, #84, #4778 ) ;
#6028=ORIENTED_EDGE ( 'NONE', *, *, #241, .T. ) ;
#6034=FACE_BOUND ( 'NONE', #1072, .T. ) ;
#6038=ORIENTED_EDGE ( 'NONE', *, *, #3869, .F. ) ;
#6042=VECTOR ( 'NONE', #2665, 39.37007874015748854 ) ;
#6051=DIRECTION ( 'NONE',  ( 0.000000000000000000, 0.000000000000000000, -1.000000000000000000 ) ) ;
#6080=EDGE_CURVE ( 'NONE', #801, #9252, #2026, .T. ) ;
#6097=LINE ( 'NONE', #13108, #8194 ) ;
#6119=CYLINDRICAL_SURFACE ( 'NONE', #12570, 0.9499999999999988454 ) ;
#6123=AXIS2_PLACEMENT_3D ( 'NONE', #14055, #9264, #8041 ) ;
#6137=ORIENTED_EDGE ( 'NONE', *, *, #1226, .T. ) ;
#6139=VECTOR ( 'NONE', #12665, 39.37007874015748854 ) ;
#6145=DIRECTION ( 'NONE',  ( 0.000000000000000000, 0.000000000000000000, 1.000000000000000000 ) ) ;
#6186=FACE_OUTER_BOUND ( 'NONE', #8244, .T. ) ;
#6220=ORIENTED_EDGE ( 'NONE', *, *, #5349, .T. ) ;
#6223=AXIS2_PLACEMENT_3D ( 'NONE', #10788, #350, #1727 ) ;
#6243=DIRECTION ( 'NONE',  ( 0.000000000000000000, 0.000000000000000000, 1.000000000000000000 ) ) ;
#6249=AXIS2_PLACEMENT_3D ( 'NONE', #8735, #13230, #14396 ) ;
#6272=LINE ( 'NONE', #9713, #4716 ) ;
#6284=CYLINDRICAL_SURFACE ( 'NONE', #12084, 0.4849999999999995981 ) ;
#6288=EDGE_CURVE ( 'NONE', #7285, #3185, #8414, .T. ) ;
#6289=VECTOR ( 'NONE', #3027, 39.37007874015748143 ) ;
#6297=CYLINDRICAL_SURFACE ( 'NONE', #6249, 0.1899999999999996136 ) ;
#6316=DIRECTION ( 'NONE',  ( -0.000000000000000000, -1.000000000000000000, -0.000000000000000000 ) ) ;
#6329=ORIENTED_EDGE ( 'NONE', *, *, #5430, .F. ) ;
#6337=DIRECTION ( 'NONE',  ( -0.000000000000000000, -1.000000000000000000, -0.000000000000000000 ) ) ;
#6340=CARTESIAN_POINT ( 'NONE',  ( 4.769268701363833074, 3.137999999999999901, 0.3249191361593796734 ) ) ;
#6342=EDGE_CURVE ( 'NONE', #12132, #9031, #14834, .T. ) ;
#6347=FACE_OUTER_BOUND ( 'NONE', #2543, .T. ) ;
#6368=EDGE_LOOP ( 'NONE', ( #8865, #1549 ) ) ;
#6394=DIRECTION ( 'NONE',  ( 0.000000000000000000, 1.000000000000000000, 0.000000000000000000 ) ) ;
#6411=CARTESIAN_POINT ( 'NONE',  ( 4.344846310392954436, 3.567999999999999616, 1.491010071662831393 ) ) ;
#6420=EDGE_CURVE ( 'NONE', #5828, #5637, #12554, .T. ) ;
#6442=CARTESIAN_POINT ( 'NONE',  ( 3.874999999999999556, 3.567999999999999616, -1.320000000000000062 ) ) ;
#6454=( NAMED_UNIT ( * ) PLANE_ANGLE_UNIT ( ) SI_UNIT ( $, .RADIAN. ) );
#6469=EDGE_CURVE ( 'NONE', #5312, #7123, #3219, .T. ) ;
#6470=ORIENTED_EDGE ( 'NONE', *, *, #4086, .F. ) ;
#6473=AXIS2_PLACEMENT_3D ( 'NONE', #9843, #8563, #8697 ) ;
#6493=DIRECTION ( 'NONE',  ( 0.000000000000000000, 0.000000000000000000, 1.000000000000000000 ) ) ;
#6494=ORIENTED_EDGE ( 'NONE', *, *, #9889, .T. ) ;
#6504=DIRECTION ( 'NONE',  ( 0.000000000000000000, 0.000000000000000000, 1.000000000000000000 ) ) ;
#6514=CARTESIAN_POINT ( 'NONE',  ( 2.980731298636167370, 3.567999999999999616, 0.3249191361593796734 ) ) ;
#6542=CONICAL_SURFACE ( 'NONE', #2863, 0.2224999999999996148, 0.7853981633974446153 ) ;
#6544=PRODUCT ( 'Thermostate Flange', 'Thermostate Flange', '', ( #2666 ) ) ;
#6586=LINE ( 'NONE', #234, #14535 ) ;
#6603=CARTESIAN_POINT ( 'NONE',  ( 4.769268701363833074, 3.567999999999999616, -0.3249191361593797289 ) ) ;
#6605=AXIS2_PLACEMENT_3D ( 'NONE', #4973, #8490, #8567 ) ;
#6619=ORIENTED_EDGE ( 'NONE', *, *, #11706, .F. ) ;
#6634=DIRECTION ( 'NONE',  ( 0.000000000000000000, 0.000000000000000000, -1.000000000000000000 ) ) ;
#6653=LENGTH_MEASURE_WITH_UNIT ( LENGTH_MEASURE( 0.02539999999999999897 ), #7572 );
#6661=EDGE_CURVE ( 'NONE', #8969, #4411, #2302, .T. ) ;
#6670=CONICAL_SURFACE ( 'NONE', #51, 0.2224999999999996148, 0.7853981633974446153 ) ;
#6673=CARTESIAN_POINT ( 'NONE',  ( 3.875000000000000000, 3.535499999999999865, 0.000000000000000000 ) ) ;
#6674=CONICAL_SURFACE ( 'NONE', #776, 0.2225000000000012523, 0.7853981633974446153 ) ;
#6689=CARTESIAN_POINT ( 'NONE',  ( 3.405153689607044232, 3.567999999999999616, 1.491010071662831171 ) ) ;
#6690=PLANE ( 'NONE',  #8115 ) ;
#6694=VERTEX_POINT ( 'NONE', #9717 ) ;
#6726=VERTEX_POINT ( 'NONE', #11930 ) ;
#6733=CARTESIAN_POINT ( 'NONE',  ( 3.875000000000000000, 3.137999999999999901, 0.5174999999999995159 ) ) ;
#6843=CIRCLE ( 'NONE', #11965, 0.4849999999999995981 ) ;
#6848=ADVANCED_FACE ( 'NONE', ( #5497, #14746, #4497, #7630 ), #12291, .T. ) ;
#6852=ORIENTED_EDGE ( 'NONE', *, *, #8587, .T. ) ;
#6861=EDGE_CURVE ( 'NONE', #282, #7304, #12523, .T. ) ;
#6873=DIRECTION ( 'NONE',  ( 0.000000000000000000, 0.000000000000000000, 1.000000000000000000 ) ) ;
#6915=ORIENTED_EDGE ( 'NONE', *, *, #422, .F. ) ;
#6959=DIRECTION ( 'NONE',  ( 0.000000000000000000, 1.000000000000000000, 0.000000000000000000 ) ) ;
#7003=EDGE_CURVE ( 'NONE', #6726, #8646, #2279, .T. ) ;
#7023=ORIENTED_EDGE ( 'NONE', *, *, #5430, .T. ) ;
#7030=EDGE_CURVE ( 'NONE', #11461, #9235, #14983, .T. ) ;
#7079=CARTESIAN_POINT ( 'NONE',  ( 3.874999999999999556, 3.137999999999999901, -1.542500000000001315 ) ) ;
#7087=CARTESIAN_POINT ( 'NONE',  ( 3.874999999999999556, 3.567999999999999616, 1.320000000000000062 ) ) ;
#7098=ORIENTED_EDGE ( 'NONE', *, *, #14271, .F. ) ;
#7099=VECTOR ( 'NONE', #683, 39.37007874015748143 ) ;
#7123=VERTEX_POINT ( 'NONE', #2937 ) ;
#7160=ORIENTED_EDGE ( 'NONE', *, *, #696, .F. ) ;
#7175=DIRECTION ( 'NONE',  ( 0.000000000000000000, 0.000000000000000000, 1.000000000000000000 ) ) ;
#7180=CARTESIAN_POINT ( 'NONE',  ( 3.874999999999999556, 3.170500000000001428, -1.509999999999999787 ) ) ;
#7209=DIRECTION ( 'NONE',  ( 0.3420201433256627732, 0.000000000000000000, 0.9396926207859105373 ) ) ;
#7224=ADVANCED_FACE ( 'NONE', ( #923 ), #8933, .F. ) ;
#7235=AXIS2_PLACEMENT_3D ( 'NONE', #10204, #3469, #8072 ) ;
#7277=EDGE_CURVE ( 'NONE', #11902, #8264, #121, .T. ) ;
#7285=VERTEX_POINT ( 'NONE', #10429 ) ;
#7293=AXIS2_PLACEMENT_3D ( 'NONE', #1543, #7594, #9971 ) ;
#7303=CARTESIAN_POINT ( 'NONE',  ( 3.875000000000000000, 3.137999999999999901, 0.000000000000000000 ) ) ;
#7304=VERTEX_POINT ( 'NONE', #1466 ) ;
#7321=EDGE_LOOP ( 'NONE', ( #9428, #4293, #3803, #9936 ) ) ;
#7335=ORIENTED_EDGE ( 'NONE', *, *, #10637, .F. ) ;
#7357=DIRECTION ( 'NONE',  ( -0.000000000000000000, -1.000000000000000000, -0.000000000000000000 ) ) ;
#7358=DIRECTION ( 'NONE',  ( 0.000000000000000000, 0.000000000000000000, 1.000000000000000000 ) ) ;
#7369=DIRECTION ( 'NONE',  ( -0.000000000000000000, -1.000000000000000000, -0.000000000000000000 ) ) ;
#7394=EDGE_CURVE ( 'NONE', #11919, #11196, #11884, .T. ) ;
#7407=EDGE_CURVE ( 'NONE', #3954, #11196, #9906, .T. ) ;
#7437=DIRECTION ( 'NONE',  ( -0.000000000000000000, -1.000000000000000000, -0.000000000000000000 ) ) ;
#7459=ADVANCED_FACE ( 'NONE', ( #2769 ), #675, .T. ) ;
#7482=CIRCLE ( 'NONE', #1840, 0.1899999999999996136 ) ;
#7501=DIRECTION ( 'NONE',  ( -0.000000000000000000, -1.000000000000000000, -0.000000000000000000 ) ) ;
#7515=DIRECTION ( 'NONE',  ( 0.000000000000000000, 0.000000000000000000, 1.000000000000000000 ) ) ;
#7520=DIRECTION ( 'NONE',  ( 0.000000000000000000, 0.000000000000000000, -1.000000000000000000 ) ) ;
#7534=AXIS2_PLACEMENT_3D ( 'NONE', #739, #7501, #6504 ) ;
#7536=EDGE_CURVE ( 'NONE', #4996, #13246, #8687, .T. ) ;
#7537=ADVANCED_FACE ( 'NONE', ( #11026 ), #12096, .T. ) ;
#7545=ADVANCED_FACE ( 'NONE', ( #4067 ), #6297, .F. ) ;
#7547=EDGE_LOOP ( 'NONE', ( #11464, #7855, #1586, #13757 ) ) ;
#7569=EDGE_CURVE ( 'NONE', #3205, #287, #7719, .T. ) ;
#7572=( LENGTH_UNIT ( ) NAMED_UNIT ( * ) SI_UNIT ( $, .METRE. ) );
#7591=EDGE_CURVE ( 'NONE', #9235, #754, #13457, .T. ) ;
#7594=DIRECTION ( 'NONE',  ( -0.000000000000000000, -1.000000000000000000, -0.000000000000000000 ) ) ;
#7596=DIRECTION ( 'NONE',  ( -0.000000000000000000, -1.000000000000000000, -0.000000000000000000 ) ) ;
#7630=FACE_OUTER_BOUND ( 'NONE', #5308, .T. ) ;
#7678=VERTEX_POINT ( 'NONE', #10266 ) ;
#7719=CIRCLE ( 'NONE', #10413, 0.9499999999999988454 ) ;
#7734=DIRECTION ( 'NONE',  ( 0.3420201433256620516, 0.000000000000000000, 0.9396926207859108704 ) ) ;
#7740=EDGE_CURVE ( 'NONE', #7304, #282, #7482, .T. ) ;
#7749=CARTESIAN_POINT ( 'NONE',  ( 4.344846310392954436, 3.137999999999999901, 1.491010071662831393 ) ) ;
#7756=CARTESIAN_POINT ( 'NONE',  ( 3.874999999999999556, 3.137999999999999901, -1.320000000000000062 ) ) ;
#7761=FACE_OUTER_BOUND ( 'NONE', #5290, .T. ) ;
#7802=ORIENTED_EDGE ( 'NONE', *, *, #995, .T. ) ;
#7836=EDGE_CURVE ( 'NONE', #9252, #801, #11386, .T. ) ;
#7851=CARTESIAN_POINT ( 'NONE',  ( 3.874999999999999556, 3.567999999999999616, -1.097499999999999920 ) ) ;
#7855=ORIENTED_EDGE ( 'NONE', *, *, #1226, .F. ) ;
#7865=ADVANCED_FACE ( 'NONE', ( #13068 ), #8286, .F. ) ;
#7871=( NAMED_UNIT ( * ) SI_UNIT ( $, .STERADIAN. ) SOLID_ANGLE_UNIT ( ) );
#7879=AXIS2_PLACEMENT_3D ( 'NONE', #11024, #9733, #6145 ) ;
#7892=STYLED_ITEM('',(#15178),#491);
#7900=DIRECTION ( 'NONE',  ( -0.000000000000000000, -1.000000000000000000, -0.000000000000000000 ) ) ;
#7954=DIRECTION ( 'NONE',  ( 0.000000000000000000, 1.000000000000000000, 0.000000000000000000 ) ) ;
#7985=ORIENTED_EDGE ( 'NONE', *, *, #12329, .T. ) ;
#7995=EDGE_CURVE ( 'NONE', #8969, #7285, #14443, .T. ) ;
#8041=DIRECTION ( 'NONE',  ( 0.000000000000000000, 0.000000000000000000, 1.000000000000000000 ) ) ;
#8067=AXIS2_PLACEMENT_3D ( 'NONE', #1858, #6394, #6243 ) ;
#8072=DIRECTION ( 'NONE',  ( 0.000000000000000000, 0.000000000000000000, 1.000000000000000000 ) ) ;
#8115=AXIS2_PLACEMENT_3D ( 'NONE', #12487, #2002, #5316 ) ;
#8117=CARTESIAN_POINT ( 'NONE',  ( 2.980731298636167370, 3.567999999999999616, -0.3249191361593797844 ) ) ;
#8160=ORIENTED_EDGE ( 'NONE', *, *, #6342, .T. ) ;
#8194=VECTOR ( 'NONE', #10760, 39.37007874015748143 ) ;
#8206=VERTEX_POINT ( 'NONE', #1038 ) ;
#8218=EDGE_CURVE ( 'NONE', #7678, #5059, #5890, .T. ) ;
#8237=CIRCLE ( 'NONE', #14805, 0.2225000000000012523 ) ;
#8244=EDGE_LOOP ( 'NONE', ( #11487, #6329, #12769, #5909 ) ) ;
#8262=ORIENTED_EDGE ( 'NONE', *, *, #6661, .T. ) ;
#8264=VERTEX_POINT ( 'NONE', #12978 ) ;
#8282=CIRCLE ( 'NONE', #415, 0.1899999999999996136 ) ;
#8286=PLANE ( 'NONE',  #11889 ) ;
#8295=CARTESIAN_POINT ( 'NONE',  ( 3.874999999999999556, 3.137999999999999901, 1.097500000000000586 ) ) ;
#8300=CONICAL_SURFACE ( 'NONE', #10234, 0.5174999999999995159, 0.7853981633974514986 ) ;
#8334=ORIENTED_EDGE ( 'NONE', *, *, #7277, .F. ) ;
#8350=ORIENTED_EDGE ( 'NONE', *, *, #10671, .F. ) ;
#8362=CARTESIAN_POINT ( 'NONE',  ( 3.874999999999999556, 3.567999999999999616, 1.320000000000000062 ) ) ;
#8366=DIRECTION ( 'NONE',  ( 0.000000000000000000, 0.000000000000000000, 1.000000000000000000 ) ) ;
#8387=CIRCLE ( 'NONE', #10326, 0.2224999999999996148 ) ;
#8390=ORIENTED_EDGE ( 'NONE', *, *, #849, .T. ) ;
#8397=CARTESIAN_POINT ( 'NONE',  ( 3.875000000000000000, 3.170499999999999208, 0.000000000000000000 ) ) ;
#8403=AXIS2_PLACEMENT_3D ( 'NONE', #9555, #3805, #14199 ) ;
#8412=FACE_OUTER_BOUND ( 'NONE', #13573, .T. ) ;
#8414=CIRCLE ( 'NONE', #10120, 0.5000000000000001110 ) ;
#8418=PLANE ( 'NONE',  #6605 ) ;
#8424=AXIS2_PLACEMENT_3D ( 'NONE', #5062, #7358, #1521 ) ;
#8429=ORIENTED_EDGE ( 'NONE', *, *, #849, .F. ) ;
#8441=ORIENTED_EDGE ( 'NONE', *, *, #975, .T. ) ;
#8449=ORIENTED_EDGE ( 'NONE', *, *, #5681, .F. ) ;
#8490=DIRECTION ( 'NONE',  ( 0.9396926207859108704, 0.000000000000000000, -0.3420201433256620516 ) ) ;
#8525=ORIENTED_EDGE ( 'NONE', *, *, #11706, .T. ) ;
#8537=VECTOR ( 'NONE', #11450, 39.37007874015748143 ) ;
#8563=DIRECTION ( 'NONE',  ( 0.000000000000000000, 1.000000000000000000, 0.000000000000000000 ) ) ;
#8567=DIRECTION ( 'NONE',  ( -0.3420201433256620516, 0.000000000000000000, -0.9396926207859108704 ) ) ;
#8587=EDGE_CURVE ( 'NONE', #7304, #8264, #1789, .T. ) ;
#8592=DIRECTION ( 'NONE',  ( -0.3420201433256628287, 0.000000000000000000, -0.9396926207859105373 ) ) ;
#8602=VECTOR ( 'NONE', #6316, 39.37007874015748143 ) ;
#8604=DIRECTION ( 'NONE',  ( 0.000000000000000000, 0.000000000000000000, -1.000000000000000000 ) ) ;
#8646=VERTEX_POINT ( 'NONE', #7851 ) ;
#8687=CIRCLE ( 'NONE', #10654, 0.2225000000000001421 ) ;
#8697=DIRECTION ( 'NONE',  ( 0.000000000000000000, 0.000000000000000000, 1.000000000000000000 ) ) ;
#8735=CARTESIAN_POINT ( 'NONE',  ( 3.874999999999999556, 3.567999999999999616, -1.320000000000000062 ) ) ;
#8745=DIRECTION ( 'NONE',  ( -0.000000000000000000, -1.000000000000000000, -0.000000000000000000 ) ) ;
#8765=VECTOR ( 'NONE', #1748, 39.37007874015748143 ) ;
#8781=DIRECTION ( 'NONE',  ( 0.000000000000000000, 0.7071067811865441310, 0.7071067811865509034 ) ) ;
#8788=CARTESIAN_POINT ( 'NONE',  ( 3.874999999999999556, 3.535499999999999421, 1.130000000000000560 ) ) ;
#8819=AXIS2_PLACEMENT_3D ( 'NONE', #1259, #5946, #3422 ) ;
#8833=ORIENTED_EDGE ( 'NONE', *, *, #14542, .T. ) ;
#8860=CARTESIAN_POINT ( 'NONE',  ( 4.344846310392954436, 3.137999999999999901, 1.491010071662831393 ) ) ;
#8865=ORIENTED_EDGE ( 'NONE', *, *, #7836, .T. ) ;
#8872=CARTESIAN_POINT ( 'NONE',  ( 3.875000000000000000, 3.567999999999999616, 0.5175000000000000711 ) ) ;
#8901=APPLICATION_CONTEXT ( 'automotive_design' ) ;
#8914=AXIS2_PLACEMENT_3D ( 'NONE', #14328, #7596, #8604 ) ;
#8932=CARTESIAN_POINT ( 'NONE',  ( 3.875000000000000000, 3.535499999999999865, -0.4849999999999995981 ) ) ;
#8933=CONICAL_SURFACE ( 'NONE', #7235, 0.4849999999999995981, 0.7853981633974598253 ) ;
#8934=DIRECTION ( 'NONE',  ( 0.000000000000000000, 1.000000000000000000, 0.000000000000000000 ) ) ;
#8937=CARTESIAN_POINT ( 'NONE',  ( 3.874999999999999556, 3.137999999999999901, 1.320000000000000062 ) ) ;
#8951=ORIENTED_EDGE ( 'NONE', *, *, #2361, .T. ) ;
#8956=EDGE_CURVE ( 'NONE', #8206, #3175, #6097, .T. ) ;
#8969=VERTEX_POINT ( 'NONE', #6689 ) ;
#8994=EDGE_CURVE ( 'NONE', #282, #11902, #13474, .T. ) ;
#9020=DIRECTION ( 'NONE',  ( -0.000000000000000000, -1.000000000000000000, -0.000000000000000000 ) ) ;
#9031=VERTEX_POINT ( 'NONE', #2081 ) ;
#9034=CONICAL_SURFACE ( 'NONE', #2434, 0.1899999999999996136, 0.7853981633974530530 ) ;
#9045=DIRECTION ( 'NONE',  ( 0.000000000000000000, 0.000000000000000000, -1.000000000000000000 ) ) ;
#9114=EDGE_LOOP ( 'NONE', ( #2662, #15017 ) ) ;
#9115=ORIENTED_EDGE ( 'NONE', *, *, #11032, .F. ) ;
#9119=( GEOMETRIC_REPRESENTATION_CONTEXT ( 3 ) GLOBAL_UNCERTAINTY_ASSIGNED_CONTEXT ( ( #13650 ) ) GLOBAL_UNIT_ASSIGNED_CONTEXT ( ( #9552, #6454, #9821 ) ) REPRESENTATION_CONTEXT ( 'NONE', 'WORKASPACE' ) );
#9158=CARTESIAN_POINT ( 'NONE',  ( 3.874999999999999556, 3.137999999999999901, 1.542499999999999760 ) ) ;
#9159=LINE ( 'NONE', #14225, #13131 ) ;
#9235=VERTEX_POINT ( 'NONE', #659 ) ;
#9248=DIRECTION ( 'NONE',  ( 0.000000000000000000, 0.000000000000000000, 1.000000000000000000 ) ) ;
#9252=VERTEX_POINT ( 'NONE', #8872 ) ;
#9264=DIRECTION ( 'NONE',  ( -0.000000000000000000, -1.000000000000000000, -0.000000000000000000 ) ) ;
#9286=ADVANCED_FACE ( 'NONE', ( #5358 ), #6284, .F. ) ;
#9297=EDGE_LOOP ( 'NONE', ( #13336, #10612, #3976, #5874 ) ) ;
#9328=VERTEX_POINT ( 'NONE', #2754 ) ;
#9334=CARTESIAN_POINT ( 'NONE',  ( 3.876560711617219379, 3.567999999999999616, 0.000000000000000000 ) ) ;
#9370=ORIENTED_EDGE ( 'NONE', *, *, #7407, .F. ) ;
#9428=ORIENTED_EDGE ( 'NONE', *, *, #8956, .F. ) ;
#9433=CARTESIAN_POINT ( 'NONE',  ( 3.874999999999999556, 3.137999999999999901, 1.542499999999999760 ) ) ;
#9443=CONICAL_SURFACE ( 'NONE', #4301, 0.1899999999999996136, 0.7853981633974530530 ) ;
#9467=DIRECTION ( 'NONE',  ( 0.000000000000000000, 0.7071067811865441310, 0.7071067811865509034 ) ) ;
#9483=CARTESIAN_POINT ( 'NONE',  ( 3.874999999999999556, 3.137999999999999901, -1.320000000000000062 ) ) ;
#9534=CONICAL_SURFACE ( 'NONE', #8067, 0.4849999999999995981, 0.7853981633974598253 ) ;
#9551=ADVANCED_FACE ( 'NONE', ( #8412 ), #6119, .T. ) ;
#9552=( CONVERSION_BASED_UNIT ( 'INCH', #14121 ) LENGTH_UNIT ( ) NAMED_UNIT ( #388 ) );
#9555=CARTESIAN_POINT ( 'NONE',  ( 3.876560711617219379, 3.137999999999999901, 0.000000000000000000 ) ) ;
#9605=DIRECTION ( 'NONE',  ( 0.000000000000000000, 0.000000000000000000, 1.000000000000000000 ) ) ;
#9607=CIRCLE ( 'NONE', #7879, 0.4849999999999995981 ) ;
#9657=ADVANCED_FACE ( 'NONE', ( #6186 ), #13057, .F. ) ;
#9664=ORIENTED_EDGE ( 'NONE', *, *, #10999, .T. ) ;
#9684=VECTOR ( 'NONE', #8592, 39.37007874015748143 ) ;
#9702=DIRECTION ( 'NONE',  ( 0.000000000000000000, 0.000000000000000000, 1.000000000000000000 ) ) ;
#9713=CARTESIAN_POINT ( 'NONE',  ( 4.769268701363833074, 3.567999999999999616, -0.3249191361593797289 ) ) ;
#9717=CARTESIAN_POINT ( 'NONE',  ( 4.344846310392954436, 3.567999999999999616, -1.491010071662831171 ) ) ;
#9722=ORIENTED_EDGE ( 'NONE', *, *, #6080, .F. ) ;
#9733=DIRECTION ( 'NONE',  ( 0.000000000000000000, 1.000000000000000000, 0.000000000000000000 ) ) ;
#9735=EDGE_CURVE ( 'NONE', #8646, #6726, #14360, .T. ) ;
#9741=ORIENTED_EDGE ( 'NONE', *, *, #6288, .F. ) ;
#9745=VECTOR ( 'NONE', #9782, 39.37007874015748143 ) ;
#9752=VECTOR ( 'NONE', #11629, 39.37007874015748143 ) ;
#9778=CIRCLE ( 'NONE', #12452, 0.1899999999999996136 ) ;
#9782=DIRECTION ( 'NONE',  ( 8.659560562354973534E-17, 0.7071067811865441310, -0.7071067811865509034 ) ) ;
#9811=ORIENTED_EDGE ( 'NONE', *, *, #7569, .F. ) ;
#9821=( NAMED_UNIT ( * ) SI_UNIT ( $, .STERADIAN. ) SOLID_ANGLE_UNIT ( ) );
#9837=ORIENTED_EDGE ( 'NONE', *, *, #4120, .T. ) ;
#9843=CARTESIAN_POINT ( 'NONE',  ( 3.874999999999999556, 3.535499999999999421, -1.320000000000000062 ) ) ;
#9850=DIRECTION ( 'NONE',  ( -0.9396926207859105373, 0.000000000000000000, -0.3420201433256627732 ) ) ;
#9860=DIRECTION ( 'NONE',  ( -0.000000000000000000, -1.000000000000000000, -0.000000000000000000 ) ) ;
#9881=DIRECTION ( 'NONE',  ( 0.000000000000000000, 0.000000000000000000, -1.000000000000000000 ) ) ;
#9886=CARTESIAN_POINT ( 'NONE',  ( 3.874999999999999556, 3.535499999999999421, -1.130000000000000560 ) ) ;
#9889=EDGE_CURVE ( 'NONE', #7304, #13246, #14112, .T. ) ;
#9906=CIRCLE ( 'NONE', #12834, 0.5174999999999995159 ) ;
#9932=DIRECTION ( 'NONE',  ( 0.000000000000000000, 0.000000000000000000, 1.000000000000000000 ) ) ;
#9933=DIRECTION ( 'NONE',  ( 0.000000000000000000, 0.000000000000000000, -1.000000000000000000 ) ) ;
#9936=ORIENTED_EDGE ( 'NONE', *, *, #14541, .F. ) ;
#9971=DIRECTION ( 'NONE',  ( 0.000000000000000000, 0.000000000000000000, -1.000000000000000000 ) ) ;
#10004=ORIENTED_EDGE ( 'NONE', *, *, #2656, .F. ) ;
#10042=DIRECTION ( 'NONE',  ( 0.000000000000000000, 0.000000000000000000, 1.000000000000000000 ) ) ;
#10044=CARTESIAN_POINT ( 'NONE',  ( 3.874999999999999556, 3.567999999999999616, -1.320000000000000062 ) ) ;
#10056=ORIENTED_EDGE ( 'NONE', *, *, #8956, .T. ) ;
#10057=ORIENTED_EDGE ( 'NONE', *, *, #5323, .F. ) ;
#10076=CARTESIAN_POINT ( 'NONE',  ( 3.405153689607044232, 3.137999999999999901, -1.491010071662831171 ) ) ;
#10120=AXIS2_PLACEMENT_3D ( 'NONE', #15065, #7954, #5591 ) ;
#10143=ORIENTED_EDGE ( 'NONE', *, *, #11568, .F. ) ;
#10178=CIRCLE ( 'NONE', #4528, 0.5000000000000000000 ) ;
#10185=ORIENTED_EDGE ( 'NONE', *, *, #11564, .T. ) ;
#10204=CARTESIAN_POINT ( 'NONE',  ( 3.875000000000000000, 3.535499999999999865, 0.000000000000000000 ) ) ;
#10208=CARTESIAN_POINT ( 'NONE',  ( 3.874999999999999556, 3.170500000000001428, -1.320000000000000062 ) ) ;
#10230=LINE ( 'NONE', #13956, #8537 ) ;
#10234=AXIS2_PLACEMENT_3D ( 'NONE', #13160, #7369, #4062 ) ;
#10241=EDGE_LOOP ( 'NONE', ( #11986, #1034, #10396, #13402 ) ) ;
#10249=AXIS2_PLACEMENT_3D ( 'NONE', #6673, #4385, #7515 ) ;
#10266=CARTESIAN_POINT ( 'NONE',  ( 3.875000000000000000, 3.535499999999999865, -0.4849999999999995981 ) ) ;
#10324=DIRECTION ( 'NONE',  ( -0.000000000000000000, -1.000000000000000000, -0.000000000000000000 ) ) ;
#10326=AXIS2_PLACEMENT_3D ( 'NONE', #12314, #14918, #13752 ) ;
#10364=VECTOR ( 'NONE', #926, 39.37007874015748143 ) ;
#10396=ORIENTED_EDGE ( 'NONE', *, *, #975, .F. ) ;
#10413=AXIS2_PLACEMENT_3D ( 'NONE', #14620, #1831, #4154 ) ;
#10416=ORIENTED_EDGE ( 'NONE', *, *, #7591, .F. ) ;
#10425=EDGE_LOOP ( 'NONE', ( #1078, #10056, #12058, #3473 ) ) ;
#10427=LINE ( 'NONE', #10657, #14229 ) ;
#10429=CARTESIAN_POINT ( 'NONE',  ( 3.405153689607044232, 3.137999999999999901, 1.491010071662831171 ) ) ;
#10530=VERTEX_POINT ( 'NONE', #10076 ) ;
#10575=ORIENTED_EDGE ( 'NONE', *, *, #356, .F. ) ;
#10583=MECHANICAL_DESIGN_GEOMETRIC_PRESENTATION_REPRESENTATION('',(#7892),#9119);
#10612=ORIENTED_EDGE ( 'NONE', *, *, #2856, .F. ) ;
#10637=EDGE_CURVE ( 'NONE', #287, #9235, #5380, .T. ) ;
#10654=AXIS2_PLACEMENT_3D ( 'NONE', #5215, #7437, #10042 ) ;
#10657=CARTESIAN_POINT ( 'NONE',  ( 3.405153689607044232, 3.567999999999999616, -1.491010071662831171 ) ) ;
#10671=EDGE_CURVE ( 'NONE', #799, #7678, #3897, .T. ) ;
#10705=CARTESIAN_POINT ( 'NONE',  ( 3.873439288382781065, 3.137999999999999901, 6.065921084684207584E-32 ) ) ;
#10706=EDGE_CURVE ( 'NONE', #8264, #11613, #989, .T. ) ;
#10745=ORIENTED_EDGE ( 'NONE', *, *, #8587, .F. ) ;
#10746=DIRECTION ( 'NONE',  ( -0.000000000000000000, -1.000000000000000000, -0.000000000000000000 ) ) ;
#10758=AXIS2_PLACEMENT_3D ( 'NONE', #3362, #4741, #1049 ) ;
#10759=DIRECTION ( 'NONE',  ( -0.000000000000000000, -1.000000000000000000, -0.000000000000000000 ) ) ;
#10760=DIRECTION ( 'NONE',  ( 8.659560562354900811E-17, -0.7071067811865501263, 0.7071067811865449082 ) ) ;
#10765=DIRECTION ( 'NONE',  ( 0.000000000000000000, 0.000000000000000000, 1.000000000000000000 ) ) ;
#10781=DIRECTION ( 'NONE',  ( 0.000000000000000000, 0.000000000000000000, 1.000000000000000000 ) ) ;
#10788=CARTESIAN_POINT ( 'NONE',  ( 3.874999999999999556, 3.567999999999999616, 1.320000000000000062 ) ) ;
#10808=DIRECTION ( 'NONE',  ( 0.000000000000000000, 1.000000000000000000, 0.000000000000000000 ) ) ;
#10816=FACE_OUTER_BOUND ( 'NONE', #7321, .T. ) ;
#10822=EDGE_LOOP ( 'NONE', ( #14411, #11776, #12910, #13767 ) ) ;
#10883=EDGE_LOOP ( 'NONE', ( #4560, #6852, #9664, #5769 ) ) ;
#10904=CARTESIAN_POINT ( 'NONE',  ( 3.874999999999999556, 3.567999999999999616, 1.097499999999999920 ) ) ;
#10931=DIRECTION ( 'NONE',  ( -0.3420201433256628287, 0.000000000000000000, -0.9396926207859105373 ) ) ;
#10951=LINE ( 'NONE', #5147, #5104 ) ;
#10962=VERTEX_POINT ( 'NONE', #8295 ) ;
#10972=CYLINDRICAL_SURFACE ( 'NONE', #8914, 0.1899999999999996136 ) ;
#10995=ORIENTED_EDGE ( 'NONE', *, *, #3381, .T. ) ;
#10999=EDGE_CURVE ( 'NONE', #8264, #11902, #2892, .T. ) ;
#11014=EDGE_CURVE ( 'NONE', #799, #9252, #14756, .T. ) ;
#11024=CARTESIAN_POINT ( 'NONE',  ( 3.875000000000000000, 3.535499999999999865, 0.000000000000000000 ) ) ;
#11026=FACE_OUTER_BOUND ( 'NONE', #9297, .T. ) ;
#11030=DIRECTION ( 'NONE',  ( -0.000000000000000000, -1.000000000000000000, -0.000000000000000000 ) ) ;
#11032=EDGE_CURVE ( 'NONE', #754, #7123, #921, .T. ) ;
#11048=VECTOR ( 'NONE', #7734, 39.37007874015748854 ) ;
#11076=ORIENTED_EDGE ( 'NONE', *, *, #7740, .T. ) ;
#11094=CARTESIAN_POINT ( 'NONE',  ( 3.875000000000000000, 3.567999999999999616, -0.5175000000000000711 ) ) ;
#11111=CONICAL_SURFACE ( 'NONE', #4275, 0.1899999999999996136, 0.7853981633974530530 ) ;
#11147=CARTESIAN_POINT ( 'NONE',  ( 4.769268701363833074, 3.567999999999999616, -0.3249191361593797289 ) ) ;
#11158=( CONVERSION_BASED_UNIT ( 'INCH', #6653 ) LENGTH_UNIT ( ) NAMED_UNIT ( #13197 ) );
#11163=CARTESIAN_POINT ( 'NONE',  ( 3.875000000000000000, 3.535499999999999865, 0.4849999999999995981 ) ) ;
#11175=FACE_OUTER_BOUND ( 'NONE', #1480, .T. ) ;
#11181=LINE ( 'NONE', #4668, #7099 ) ;
#11196=VERTEX_POINT ( 'NONE', #6733 ) ;
#11319=LINE ( 'NONE', #588, #13635 ) ;
#11343=DIRECTION ( 'NONE',  ( 0.000000000000000000, 1.000000000000000000, 0.000000000000000000 ) ) ;
#11386=CIRCLE ( 'NONE', #4804, 0.5175000000000000711 ) ;
#11450=DIRECTION ( 'NONE',  ( 0.3420201433256627732, 0.000000000000000000, -0.9396926207859105373 ) ) ;
#11461=VERTEX_POINT ( 'NONE', #6340 ) ;
#11464=ORIENTED_EDGE ( 'NONE', *, *, #6288, .T. ) ;
#11481=DIRECTION ( 'NONE',  ( -0.000000000000000000, -1.000000000000000000, -0.000000000000000000 ) ) ;
#11487=ORIENTED_EDGE ( 'NONE', *, *, #4113, .F. ) ;
#11564=EDGE_CURVE ( 'NONE', #4411, #3205, #10230, .T. ) ;
#11568=EDGE_CURVE ( 'NONE', #13246, #4996, #12919, .T. ) ;
#11572=CIRCLE ( 'NONE', #3513, 0.5174999999999995159 ) ;
#11591=EDGE_CURVE ( 'NONE', #5637, #3175, #12199, .T. ) ;
#11605=DIRECTION ( 'NONE',  ( 0.000000000000000000, 1.000000000000000000, 0.000000000000000000 ) ) ;
#11613=VERTEX_POINT ( 'NONE', #9158 ) ;
#11629=DIRECTION ( 'NONE',  ( -0.000000000000000000, -1.000000000000000000, -0.000000000000000000 ) ) ;
#11640=AXIS2_PLACEMENT_3D ( 'NONE', #6411, #9850, #5259 ) ;
#11659=ADVANCED_FACE ( 'NONE', ( #15116 ), #9034, .F. ) ;
#11706=EDGE_CURVE ( 'NONE', #11919, #5059, #6843, .T. ) ;
#11713=LINE ( 'NONE', #4743, #9752 ) ;
#11776=ORIENTED_EDGE ( 'NONE', *, *, #12290, .F. ) ;
#11788=DIRECTION ( 'NONE',  ( -0.000000000000000000, -1.000000000000000000, -0.000000000000000000 ) ) ;
#11812=ADVANCED_FACE ( 'NONE', ( #12268 ), #9534, .F. ) ;
#11827=CARTESIAN_POINT ( 'NONE',  ( 3.874999999999999556, 3.535499999999999421, 1.509999999999999787 ) ) ;
#11838=VECTOR ( 'NONE', #12340, 39.37007874015748143 ) ;
#11884=LINE ( 'NONE', #14239, #14544 ) ;
#11889=AXIS2_PLACEMENT_3D ( 'NONE', #2530, #281, #7209 ) ;
#11902=VERTEX_POINT ( 'NONE', #13711 ) ;
#11919=VERTEX_POINT ( 'NONE', #1942 ) ;
#11927=AXIS2_PLACEMENT_3D ( 'NONE', #5203, #14603, #512 ) ;
#11930=CARTESIAN_POINT ( 'NONE',  ( 3.874999999999999556, 3.567999999999999616, -1.542500000000000204 ) ) ;
#11935=EDGE_LOOP ( 'NONE', ( #12273, #8334, #7985, #14955 ) ) ;
#11938=DIRECTION ( 'NONE',  ( 0.000000000000000000, 0.000000000000000000, 1.000000000000000000 ) ) ;
#11950=ORIENTED_EDGE ( 'NONE', *, *, #2656, .T. ) ;
#11965=AXIS2_PLACEMENT_3D ( 'NONE', #8397, #318, #10765 ) ;
#11986=ORIENTED_EDGE ( 'NONE', *, *, #1481, .T. ) ;
#12034=CARTESIAN_POINT ( 'NONE',  ( 3.874999999999999556, 3.567999999999999616, 1.542500000000000204 ) ) ;
#12046=LINE ( 'NONE', #1626, #8602 ) ;
#12056=ORIENTED_EDGE ( 'NONE', *, *, #4086, .T. ) ;
#12058=ORIENTED_EDGE ( 'NONE', *, *, #11591, .F. ) ;
#12084=AXIS2_PLACEMENT_3D ( 'NONE', #5063, #13442, #3053 ) ;
#12094=VERTEX_POINT ( 'NONE', #9886 ) ;
#12096=CYLINDRICAL_SURFACE ( 'NONE', #13555, 0.5000000000000001110 ) ;
#12112=ORIENTED_EDGE ( 'NONE', *, *, #174, .F. ) ;
#12132=VERTEX_POINT ( 'NONE', #5082 ) ;
#12199=CIRCLE ( 'NONE', #12932, 0.2225000000000012523 ) ;
#12203=ORIENTED_EDGE ( 'NONE', *, *, #8218, .T. ) ;
#12215=ADVANCED_BREP_SHAPE_REPRESENTATION ( '', ( #491, #8424 ), #12311 ) ;
#12262=EDGE_CURVE ( 'NONE', #7123, #10530, #956, .T. ) ;
#12268=FACE_OUTER_BOUND ( 'NONE', #3049, .T. ) ;
#12273=ORIENTED_EDGE ( 'NONE', *, *, #10706, .F. ) ;
#12290=EDGE_CURVE ( 'NONE', #5059, #11919, #5867, .T. ) ;
#12291=PLANE ( 'NONE',  #5704 ) ;
#12292=ORIENTED_EDGE ( 'NONE', *, *, #12402, .T. ) ;
#12297=CARTESIAN_POINT ( 'NONE',  ( 3.405153689607044232, 3.567999999999999616, 1.491010071662831171 ) ) ;
#12311=( GEOMETRIC_REPRESENTATION_CONTEXT ( 3 ) GLOBAL_UNCERTAINTY_ASSIGNED_CONTEXT ( ( #15031 ) ) GLOBAL_UNIT_ASSIGNED_CONTEXT ( ( #11158, #4051, #7871 ) ) REPRESENTATION_CONTEXT ( 'NONE', 'WORKASPACE' ) );
#12314=CARTESIAN_POINT ( 'NONE',  ( 3.874999999999999556, 3.137999999999999901, 1.320000000000000062 ) ) ;
#12329=EDGE_CURVE ( 'NONE', #11902, #10962, #11181, .T. ) ;
#12340=DIRECTION ( 'NONE',  ( -0.000000000000000000, -1.000000000000000000, -0.000000000000000000 ) ) ;
#12364=CARTESIAN_POINT ( 'NONE',  ( 4.769268701363833074, 3.567999999999999616, 0.3249191361593796734 ) ) ;
#12397=ORIENTED_EDGE ( 'NONE', *, *, #11014, .T. ) ;
#12402=EDGE_CURVE ( 'NONE', #5284, #12094, #9778, .T. ) ;
#12409=CARTESIAN_POINT ( 'NONE',  ( 3.874999999999999556, 3.137999999999999901, -1.097499999999998810 ) ) ;
#12412=ADVANCED_FACE ( 'NONE', ( #199 ), #8418, .F. ) ;
#12452=AXIS2_PLACEMENT_3D ( 'NONE', #12835, #14434, #3896 ) ;
#12454=EDGE_CURVE ( 'NONE', #9031, #12926, #15150, .T. ) ;
#12487=CARTESIAN_POINT ( 'NONE',  ( 3.405153689607044232, 3.567999999999999616, -1.491010071662831171 ) ) ;
#12523=CIRCLE ( 'NONE', #14740, 0.1899999999999996136 ) ;
#12551=DIRECTION ( 'NONE',  ( 0.000000000000000000, 0.000000000000000000, 1.000000000000000000 ) ) ;
#12554=LINE ( 'NONE', #2078, #10364 ) ;
#12570=AXIS2_PLACEMENT_3D ( 'NONE', #9334, #2444, #3590 ) ;
#12574=CARTESIAN_POINT ( 'NONE',  ( 3.873439288382781065, 3.567999999999999616, 6.065921084684207584E-32 ) ) ;
#12632=CARTESIAN_POINT ( 'NONE',  ( 3.874999999999999556, 3.137999999999999901, -1.320000000000000062 ) ) ;
#12640=AXIS2_PLACEMENT_3D ( 'NONE', #12850, #3760, #11938 ) ;
#12657=FACE_OUTER_BOUND ( 'NONE', #2198, .T. ) ;
#12663=DIRECTION ( 'NONE',  ( 0.000000000000000000, 1.000000000000000000, 0.000000000000000000 ) ) ;
#12665=DIRECTION ( 'NONE',  ( 8.659560562355030233E-17, 0.7071067811865392461, -0.7071067811865555663 ) ) ;
#12690=CARTESIAN_POINT ( 'NONE',  ( 3.875000000000000000, 3.567999999999999616, 0.000000000000000000 ) ) ;
#12737=CARTESIAN_POINT ( 'NONE',  ( 3.874999999999999556, 3.567999999999999616, 1.320000000000000062 ) ) ;
#12745=CARTESIAN_POINT ( 'NONE',  ( 3.875000000000000000, 3.567999999999999616, -0.4849999999999995981 ) ) ;
#12767=DIRECTION ( 'NONE',  ( 0.000000000000000000, 0.000000000000000000, 1.000000000000000000 ) ) ;
#12769=ORIENTED_EDGE ( 'NONE', *, *, #3869, .T. ) ;
#12782=DIRECTION ( 'NONE',  ( -0.3420201433256621071, 0.000000000000000000, 0.9396926207859108704 ) ) ;
#12798=PRODUCT_DEFINITION_FORMATION_WITH_SPECIFIED_SOURCE ( 'ANY', '', #6544, .NOT_KNOWN. ) ;
#12804=ORIENTED_EDGE ( 'NONE', *, *, #14541, .T. ) ;
#12831=FACE_OUTER_BOUND ( 'NONE', #5270, .T. ) ;
#12834=AXIS2_PLACEMENT_3D ( 'NONE', #7303, #10808, #3853 ) ;
#12835=CARTESIAN_POINT ( 'NONE',  ( 3.874999999999999556, 3.535499999999999421, -1.320000000000000062 ) ) ;
#12850=CARTESIAN_POINT ( 'NONE',  ( 3.873439288382781065, 3.567999999999999616, 6.065921084684207584E-32 ) ) ;
#12861=CARTESIAN_POINT ( 'NONE',  ( 4.344846310392954436, 3.137999999999999901, -1.491010071662831171 ) ) ;
#12870=FACE_OUTER_BOUND ( 'NONE', #10883, .T. ) ;
#12910=ORIENTED_EDGE ( 'NONE', *, *, #4592, .T. ) ;
#12919=CIRCLE ( 'NONE', #14394, 0.2225000000000001421 ) ;
#12926=VERTEX_POINT ( 'NONE', #5241 ) ;
#12932=AXIS2_PLACEMENT_3D ( 'NONE', #5645, #12663, #6873 ) ;
#12978=CARTESIAN_POINT ( 'NONE',  ( 3.874999999999999556, 3.170500000000000096, 1.509999999999999787 ) ) ;
#13019=AXIS2_PLACEMENT_3D ( 'NONE', #15051, #4576, #9248 ) ;
#13057=CONICAL_SURFACE ( 'NONE', #6473, 0.1899999999999996136, 0.7853981633974530530 ) ;
#13068=FACE_OUTER_BOUND ( 'NONE', #4730, .T. ) ;
#13108=CARTESIAN_POINT ( 'NONE',  ( 3.874999999999999556, 3.137999999999999901, -1.097499999999998810 ) ) ;
#13131=VECTOR ( 'NONE', #5833, 39.37007874015748143 ) ;
#13160=CARTESIAN_POINT ( 'NONE',  ( 3.875000000000000000, 3.137999999999999901, 0.000000000000000000 ) ) ;
#13169=VERTEX_POINT ( 'NONE', #14100 ) ;
#13197=DIMENSIONAL_EXPONENTS ( 1.000000000000000000, 0.000000000000000000, 0.000000000000000000, 0.000000000000000000, 0.000000000000000000, 0.000000000000000000, 0.000000000000000000 ) ;
#13202=CARTESIAN_POINT ( 'NONE',  ( 3.874999999999999556, 3.535499999999999421, -1.130000000000000560 ) ) ;
#13229=ADVANCED_FACE ( 'NONE', ( #2932 ), #179, .F. ) ;
#13230=DIRECTION ( 'NONE',  ( -0.000000000000000000, -1.000000000000000000, -0.000000000000000000 ) ) ;
#13246=VERTEX_POINT ( 'NONE', #12034 ) ;
#13336=ORIENTED_EDGE ( 'NONE', *, *, #6469, .F. ) ;
#13339=CARTESIAN_POINT ( 'NONE',  ( 3.875000000000000000, 3.137999999999999901, -0.5174999999999995159 ) ) ;
#13351=ADVANCED_FACE ( 'NONE', ( #3165 ), #11111, .F. ) ;
#13359=ORIENTED_EDGE ( 'NONE', *, *, #6469, .T. ) ;
#13379=AXIS2_PLACEMENT_3D ( 'NONE', #1645, #6337, #9702 ) ;
#13402=ORIENTED_EDGE ( 'NONE', *, *, #4178, .T. ) ;
#13442=DIRECTION ( 'NONE',  ( -0.000000000000000000, -1.000000000000000000, -0.000000000000000000 ) ) ;
#13457=LINE ( 'NONE', #376, #9684 ) ;
#13474=LINE ( 'NONE', #3016, #11838 ) ;
#13489=DIRECTION ( 'NONE',  ( -0.000000000000000000, -1.000000000000000000, -0.000000000000000000 ) ) ;
#13497=LINE ( 'NONE', #8932, #6139 ) ;
#13499=CARTESIAN_POINT ( 'NONE',  ( 3.874999999999999556, 3.535499999999999421, -1.320000000000000062 ) ) ;
#13543=CARTESIAN_POINT ( 'NONE',  ( 3.875000000000000000, 3.567999999999999616, 0.000000000000000000 ) ) ;
#13549=ORIENTED_EDGE ( 'NONE', *, *, #4592, .F. ) ;
#13555=AXIS2_PLACEMENT_3D ( 'NONE', #6442, #594, #9881 ) ;
#13573=EDGE_LOOP ( 'NONE', ( #1944, #7335, #9811, #6220 ) ) ;
#13625=DIRECTION ( 'NONE',  ( 0.000000000000000000, 0.000000000000000000, -1.000000000000000000 ) ) ;
#13631=DIRECTION ( 'NONE',  ( 0.000000000000000000, 0.000000000000000000, 1.000000000000000000 ) ) ;
#13635=VECTOR ( 'NONE', #819, 39.37007874015748854 ) ;
#13650=UNCERTAINTY_MEASURE_WITH_UNIT (LENGTH_MEASURE( 1.000000000000000082E-05 ), #9552, 'distance_accuracy_value', 'NONE');
#13666=CARTESIAN_POINT ( 'NONE',  ( 3.874999999999999556, 3.567999999999999616, -1.320000000000000062 ) ) ;
#13700=DIRECTION ( 'NONE',  ( 0.000000000000000000, 0.000000000000000000, -1.000000000000000000 ) ) ;
#13705=ORIENTED_EDGE ( 'NONE', *, *, #7277, .T. ) ;
#13711=CARTESIAN_POINT ( 'NONE',  ( 3.874999999999999556, 3.170500000000000096, 1.130000000000000560 ) ) ;
#13726=DIRECTION ( 'NONE',  ( -0.000000000000000000, -1.000000000000000000, -0.000000000000000000 ) ) ;
#13752=DIRECTION ( 'NONE',  ( 0.000000000000000000, 0.000000000000000000, 1.000000000000000000 ) ) ;
#13757=ORIENTED_EDGE ( 'NONE', *, *, #7995, .T. ) ;
#13767=ORIENTED_EDGE ( 'NONE', *, *, #28, .F. ) ;
#13828=DIRECTION ( 'NONE',  ( 0.000000000000000000, 1.000000000000000000, 0.000000000000000000 ) ) ;
#13864=ORIENTED_EDGE ( 'NONE', *, *, #12454, .F. ) ;
#13956=CARTESIAN_POINT ( 'NONE',  ( 4.344846310392954436, 3.567999999999999616, 1.491010071662831393 ) ) ;
#14013=VECTOR ( 'NONE', #10324, 39.37007874015748143 ) ;
#14033=DIRECTION ( 'NONE',  ( 0.000000000000000000, 1.000000000000000000, 0.000000000000000000 ) ) ;
#14044=ORIENTED_EDGE ( 'NONE', *, *, #7394, .T. ) ;
#14055=CARTESIAN_POINT ( 'NONE',  ( 3.875000000000000000, 3.170499999999999208, 0.000000000000000000 ) ) ;
#14065=ORIENTED_EDGE ( 'NONE', *, *, #356, .T. ) ;
#14100=CARTESIAN_POINT ( 'NONE',  ( 3.405153689607044232, 3.567999999999999616, -1.491010071662831171 ) ) ;
#14112=LINE ( 'NONE', #11827, #2647 ) ;
#14121=LENGTH_MEASURE_WITH_UNIT ( LENGTH_MEASURE( 0.02539999999999999897 ), #15125 );
#14146=CARTESIAN_POINT ( 'NONE',  ( 3.874999999999999556, 3.535499999999999421, 1.130000000000000560 ) ) ;
#14151=FACE_OUTER_BOUND ( 'NONE', #7547, .T. ) ;
#14181=ADVANCED_FACE ( 'NONE', ( #14151 ), #3687, .T. ) ;
#14199=DIRECTION ( 'NONE',  ( 0.000000000000000000, 0.000000000000000000, 1.000000000000000000 ) ) ;
#14207=CARTESIAN_POINT ( 'NONE',  ( 3.874999999999999556, 3.137999999999999901, 1.320000000000000062 ) ) ;
#14225=CARTESIAN_POINT ( 'NONE',  ( 3.874999999999999556, 3.535499999999999421, -1.509999999999999787 ) ) ;
#14229=VECTOR ( 'NONE', #12782, 39.37007874015748143 ) ;
#14239=CARTESIAN_POINT ( 'NONE',  ( 3.875000000000000000, 3.137999999999999901, 0.5174999999999995159 ) ) ;
#14246=CLOSED_SHELL ( 'NONE', ( #7224, #1225, #13351, #3713, #2693, #606, #3042, #3341, #7545, #7459, #6848, #4453, #7537, #5172, #4761, #12412, #14181, #2718, #9551, #7865, #14929, #2968, #9286, #2962, #9657, #324, #11659, #13229, #11812 ) ) ;
#14271=EDGE_CURVE ( 'NONE', #5284, #5828, #4712, .T. ) ;
#14296=ORIENTED_EDGE ( 'NONE', *, *, #5323, .T. ) ;
#14309=ORIENTED_EDGE ( 'NONE', *, *, #8994, .T. ) ;
#14315=AXIS2_PLACEMENT_3D ( 'NONE', #8362, #1364, #6051 ) ;
#14328=CARTESIAN_POINT ( 'NONE',  ( 3.874999999999999556, 3.567999999999999616, 1.320000000000000062 ) ) ;
#14344=ORIENTED_EDGE ( 'NONE', *, *, #7591, .T. ) ;
#14353=ORIENTED_EDGE ( 'NONE', *, *, #6861, .F. ) ;
#14360=CIRCLE ( 'NONE', #13379, 0.2225000000000001421 ) ;
#14362=LINE ( 'NONE', #14146, #9745 ) ;
#14394=AXIS2_PLACEMENT_3D ( 'NONE', #12737, #13726, #3262 ) ;
#14396=DIRECTION ( 'NONE',  ( 0.000000000000000000, 0.000000000000000000, -1.000000000000000000 ) ) ;
#14411=ORIENTED_EDGE ( 'NONE', *, *, #7394, .F. ) ;
#14434=DIRECTION ( 'NONE',  ( 0.000000000000000000, 1.000000000000000000, 0.000000000000000000 ) ) ;
#14435=VECTOR ( 'NONE', #4852, 39.37007874015748143 ) ;
#14443=LINE ( 'NONE', #12297, #15058 ) ;
#14504=FACE_OUTER_BOUND ( 'NONE', #11935, .T. ) ;
#14529=CARTESIAN_POINT ( 'NONE',  ( 3.875000000000000000, 3.535499999999999865, 0.4849999999999995981 ) ) ;
#14535=VECTOR ( 'NONE', #10746, 39.37007874015748143 ) ;
#14541=EDGE_CURVE ( 'NONE', #3175, #5637, #8237, .T. ) ;
#14542=EDGE_CURVE ( 'NONE', #5828, #8206, #2094, .T. ) ;
#14544=VECTOR ( 'NONE', #2395, 39.37007874015748854 ) ;
#14603=DIRECTION ( 'NONE',  ( 0.000000000000000000, 1.000000000000000000, 0.000000000000000000 ) ) ;
#14620=CARTESIAN_POINT ( 'NONE',  ( 3.876560711617219379, 3.567999999999999616, 0.000000000000000000 ) ) ;
#14680=ORIENTED_EDGE ( 'NONE', *, *, #12329, .F. ) ;
#14740=AXIS2_PLACEMENT_3D ( 'NONE', #5424, #1803, #6493 ) ;
#14742=DIRECTION ( 'NONE',  ( 0.3420201433256627732, 0.000000000000000000, -0.9396926207859105373 ) ) ;
#14746=FACE_BOUND ( 'NONE', #9114, .T. ) ;
#14756=LINE ( 'NONE', #11163, #5099 ) ;
#14796=VECTOR ( 'NONE', #10759, 39.37007874015748143 ) ;
#14805=AXIS2_PLACEMENT_3D ( 'NONE', #7756, #11343, #13631 ) ;
#14834=LINE ( 'NONE', #8117, #14013 ) ;
#14897=CARTESIAN_POINT ( 'NONE',  ( 3.874999999999999556, 3.137999999999999901, 1.320000000000000062 ) ) ;
#14918=DIRECTION ( 'NONE',  ( 0.000000000000000000, 1.000000000000000000, 0.000000000000000000 ) ) ;
#14923=ORIENTED_EDGE ( 'NONE', *, *, #7569, .T. ) ;
#14929=ADVANCED_FACE ( 'NONE', ( #11175 ), #5379, .F. ) ;
#14955=ORIENTED_EDGE ( 'NONE', *, *, #995, .F. ) ;
#14975=ORIENTED_EDGE ( 'NONE', *, *, #3381, .F. ) ;
#14983=CIRCLE ( 'NONE', #8403, 0.9499999999999988454 ) ;
#15017=ORIENTED_EDGE ( 'NONE', *, *, #7536, .T. ) ;
#15031=UNCERTAINTY_MEASURE_WITH_UNIT (LENGTH_MEASURE( 1.000000000000000082E-05 ), #11158, 'distance_accuracy_value', 'NONE');
#15041=ORIENTED_EDGE ( 'NONE', *, *, #4178, .F. ) ;
#15051=CARTESIAN_POINT ( 'NONE',  ( 3.874999999999999556, 3.567999999999999616, -1.320000000000000062 ) ) ;
#15056=ORIENTED_EDGE ( 'NONE', *, *, #2856, .T. ) ;
#15058=VECTOR ( 'NONE', #9860, 39.37007874015748143 ) ;
#15065=CARTESIAN_POINT ( 'NONE',  ( 3.874999999999999556, 3.137999999999999901, 1.320000000000000062 ) ) ;
#15116=FACE_OUTER_BOUND ( 'NONE', #2243, .T. ) ;
#15125=( LENGTH_UNIT ( ) NAMED_UNIT ( * ) SI_UNIT ( $, .METRE. ) );
#15150=CIRCLE ( 'NONE', #467, 0.9499999999999988454 ) ;
#15172=COLOUR_RGB('Light Blue',0.38,0.62,0.78);
#15173=FILL_AREA_STYLE_COLOUR('',#15172);
#15174=FILL_AREA_STYLE('',(#15173));
#15175=SURFACE_STYLE_FILL_AREA(#15174);
#15176=SURFACE_SIDE_STYLE('',(#15175));
#15177=SURFACE_STYLE_USAGE(.BOTH.,#15176);
#15178=PRESENTATION_STYLE_ASSIGNMENT((#15177));
ENDSEC;
END-ISO-10303-21;
